ISO-10303-21;
HEADER;
/* Generated by software containing ST-Developer
 * from STEP Tools, Inc. (www.steptools.com) 
 */

FILE_DESCRIPTION(
/* description */ ('STEP AP214'),
/* implementation_level */ '2;1');

FILE_NAME(
/* name */ 'socket button head screw_iso_ISO 7380 - M4 x 12 - 12N.step',
/* time_stamp */ '2026-11-04T19:43:37-08:00',
/* author */ (''),
/* organization */ (''),
/* preprocessor_version */ 'ST-DEVELOPER v20.2',
/* originating_system */ 'Autodesk Translation Framework v15.17.0.0',
/* authorisation */ '');

FILE_SCHEMA (('AUTOMOTIVE_DESIGN { 1 0 10303 214 3 1 1 }'));
ENDSEC;

DATA;
#10=MECHANICAL_DESIGN_GEOMETRIC_PRESENTATION_REPRESENTATION('',(#135),#7627);
#59=SPHERICAL_SURFACE('',#2835,4.3249693283142);
#90=TOROIDAL_SURFACE('',#2824,2.2,0.2);
#105=SHAPE_REPRESENTATION_RELATIONSHIP('SRR','None',#7673,#114);
#114=ADVANCED_BREP_SHAPE_REPRESENTATION('',(#156),#7626);
#135=STYLED_ITEM('',(#7721),#156);
#156=MANIFOLD_SOLID_BREP('Body1',#2433);
#188=FACE_BOUND('',#632,.T.);
#189=FACE_BOUND('',#634,.T.);
#190=FACE_BOUND('',#636,.T.);
#237=PLANE('',#2837);
#238=PLANE('',#2838);
#239=PLANE('',#2839);
#240=PLANE('',#2840);
#241=PLANE('',#2841);
#242=PLANE('',#2842);
#243=PLANE('',#2843);
#244=PLANE('',#2844);
#245=PLANE('',#2845);
#246=PLANE('',#2846);
#247=PLANE('',#2847);
#248=PLANE('',#2848);
#249=PLANE('',#2849);
#250=PLANE('',#2850);
#251=PLANE('',#2851);
#306=CYLINDRICAL_SURFACE('',#2831,2.);
#307=CYLINDRICAL_SURFACE('',#2832,3.8);
#441=FACE_OUTER_BOUND('',#626,.T.);
#442=FACE_OUTER_BOUND('',#627,.T.);
#443=FACE_OUTER_BOUND('',#628,.T.);
#444=FACE_OUTER_BOUND('',#629,.T.);
#445=FACE_OUTER_BOUND('',#630,.T.);
#446=FACE_OUTER_BOUND('',#631,.T.);
#447=FACE_OUTER_BOUND('',#633,.T.);
#448=FACE_OUTER_BOUND('',#635,.T.);
#449=FACE_OUTER_BOUND('',#637,.T.);
#450=FACE_OUTER_BOUND('',#638,.T.);
#451=FACE_OUTER_BOUND('',#639,.T.);
#452=FACE_OUTER_BOUND('',#640,.T.);
#453=FACE_OUTER_BOUND('',#641,.T.);
#454=FACE_OUTER_BOUND('',#642,.T.);
#455=FACE_OUTER_BOUND('',#643,.T.);
#456=FACE_OUTER_BOUND('',#644,.T.);
#457=FACE_OUTER_BOUND('',#645,.T.);
#458=FACE_OUTER_BOUND('',#646,.T.);
#459=FACE_OUTER_BOUND('',#647,.T.);
#460=FACE_OUTER_BOUND('',#648,.T.);
#461=FACE_OUTER_BOUND('',#649,.T.);
#626=EDGE_LOOP('',(#2169,#2170,#2171,#2172,#2173,#2174,#2175,#2176));
#627=EDGE_LOOP('',(#2177,#2178,#2179,#2180));
#628=EDGE_LOOP('',(#2181,#2182,#2183,#2184));
#629=EDGE_LOOP('',(#2185,#2186,#2187,#2188));
#630=EDGE_LOOP('',(#2189,#2190,#2191,#2192));
#631=EDGE_LOOP('',(#2193));
#632=EDGE_LOOP('',(#2194));
#633=EDGE_LOOP('',(#2195));
#634=EDGE_LOOP('',(#2196,#2197,#2198,#2199,#2200,#2201));
#635=EDGE_LOOP('',(#2202));
#636=EDGE_LOOP('',(#2203));
#637=EDGE_LOOP('',(#2204));
#638=EDGE_LOOP('',(#2205,#2206,#2207,#2208,#2209));
#639=EDGE_LOOP('',(#2210,#2211,#2212,#2213,#2214));
#640=EDGE_LOOP('',(#2215,#2216,#2217,#2218,#2219));
#641=EDGE_LOOP('',(#2220,#2221,#2222,#2223,#2224));
#642=EDGE_LOOP('',(#2225,#2226,#2227,#2228,#2229));
#643=EDGE_LOOP('',(#2230,#2231,#2232,#2233,#2234));
#644=EDGE_LOOP('',(#2235,#2236,#2237));
#645=EDGE_LOOP('',(#2238,#2239,#2240));
#646=EDGE_LOOP('',(#2241,#2242,#2243));
#647=EDGE_LOOP('',(#2244,#2245,#2246));
#648=EDGE_LOOP('',(#2247,#2248,#2249));
#649=EDGE_LOOP('',(#2250,#2251,#2252));
#789=CIRCLE('',#2818,1.25);
#790=CIRCLE('',#2819,1.25);
#791=CIRCLE('',#2820,1.25);
#792=CIRCLE('',#2821,1.25);
#793=CIRCLE('',#2822,1.25);
#794=CIRCLE('',#2823,1.25);
#795=CIRCLE('',#2825,2.2);
#796=CIRCLE('',#2826,0.2);
#797=CIRCLE('',#2827,2.);
#798=CIRCLE('',#2829,2.);
#799=CIRCLE('',#2830,1.61);
#800=CIRCLE('',#2833,3.8);
#801=CIRCLE('',#2834,3.8);
#802=CIRCLE('',#2836,1.9);
#931=LINE('',#7508,#1087);
#932=LINE('',#7530,#1088);
#933=LINE('',#7533,#1089);
#934=LINE('',#7538,#1090);
#935=LINE('',#7546,#1091);
#936=LINE('',#7548,#1092);
#937=LINE('',#7550,#1093);
#938=LINE('',#7552,#1094);
#939=LINE('',#7554,#1095);
#940=LINE('',#7555,#1096);
#941=LINE('',#7560,#1097);
#942=LINE('',#7562,#1098);
#943=LINE('',#7563,#1099);
#944=LINE('',#7564,#1100);
#945=LINE('',#7566,#1101);
#946=LINE('',#7568,#1102);
#947=LINE('',#7569,#1103);
#948=LINE('',#7571,#1104);
#949=LINE('',#7573,#1105);
#950=LINE('',#7574,#1106);
#951=LINE('',#7576,#1107);
#952=LINE('',#7578,#1108);
#953=LINE('',#7579,#1109);
#954=LINE('',#7581,#1110);
#955=LINE('',#7583,#1111);
#956=LINE('',#7584,#1112);
#957=LINE('',#7586,#1113);
#958=LINE('',#7587,#1114);
#1087=VECTOR('',#3560,1732.05080756886);
#1088=VECTOR('',#3585,1.61);
#1089=VECTOR('',#3590,2.);
#1090=VECTOR('',#3595,3.8);
#1091=VECTOR('',#3604,1000.);
#1092=VECTOR('',#3605,1000.);
#1093=VECTOR('',#3606,1000.);
#1094=VECTOR('',#3607,1000.);
#1095=VECTOR('',#3608,1000.);
#1096=VECTOR('',#3609,1000.);
#1097=VECTOR('',#3616,1000.);
#1098=VECTOR('',#3617,1000.);
#1099=VECTOR('',#3618,1000.);
#1100=VECTOR('',#3619,1000.);
#1101=VECTOR('',#3622,1000.);
#1102=VECTOR('',#3623,1000.);
#1103=VECTOR('',#3624,1000.);
#1104=VECTOR('',#3627,1000.);
#1105=VECTOR('',#3628,1000.);
#1106=VECTOR('',#3629,1000.);
#1107=VECTOR('',#3632,1000.);
#1108=VECTOR('',#3633,1000.);
#1109=VECTOR('',#3634,1000.);
#1110=VECTOR('',#3637,1000.);
#1111=VECTOR('',#3638,1000.);
#1112=VECTOR('',#3639,1000.);
#1113=VECTOR('',#3642,1000.);
#1114=VECTOR('',#3643,1000.);
#1279=VERTEX_POINT('',#7506);
#1280=VERTEX_POINT('',#7507);
#1281=VERTEX_POINT('',#7509);
#1282=VERTEX_POINT('',#7511);
#1283=VERTEX_POINT('',#7513);
#1284=VERTEX_POINT('',#7515);
#1285=VERTEX_POINT('',#7517);
#1286=VERTEX_POINT('',#7521);
#1287=VERTEX_POINT('',#7523);
#1288=VERTEX_POINT('',#7527);
#1289=VERTEX_POINT('',#7529);
#1290=VERTEX_POINT('',#7535);
#1291=VERTEX_POINT('',#7537);
#1292=VERTEX_POINT('',#7541);
#1293=VERTEX_POINT('',#7544);
#1294=VERTEX_POINT('',#7545);
#1295=VERTEX_POINT('',#7547);
#1296=VERTEX_POINT('',#7549);
#1297=VERTEX_POINT('',#7551);
#1298=VERTEX_POINT('',#7553);
#1299=VERTEX_POINT('',#7559);
#1300=VERTEX_POINT('',#7561);
#1301=VERTEX_POINT('',#7567);
#1302=VERTEX_POINT('',#7572);
#1303=VERTEX_POINT('',#7577);
#1304=VERTEX_POINT('',#7582);
#1579=EDGE_CURVE('',#1279,#1280,#931,.T.);
#1580=EDGE_CURVE('',#1280,#1281,#789,.T.);
#1581=EDGE_CURVE('',#1281,#1282,#790,.T.);
#1582=EDGE_CURVE('',#1282,#1283,#791,.T.);
#1583=EDGE_CURVE('',#1283,#1284,#792,.T.);
#1584=EDGE_CURVE('',#1284,#1285,#793,.T.);
#1585=EDGE_CURVE('',#1285,#1280,#794,.T.);
#1586=EDGE_CURVE('',#1286,#1286,#795,.T.);
#1587=EDGE_CURVE('',#1286,#1287,#796,.T.);
#1588=EDGE_CURVE('',#1287,#1287,#797,.T.);
#1589=EDGE_CURVE('',#1288,#1288,#798,.T.);
#1590=EDGE_CURVE('',#1288,#1289,#932,.T.);
#1591=EDGE_CURVE('',#1289,#1289,#799,.T.);
#1592=EDGE_CURVE('',#1287,#1288,#933,.T.);
#1593=EDGE_CURVE('',#1290,#1290,#800,.T.);
#1594=EDGE_CURVE('',#1290,#1291,#934,.T.);
#1595=EDGE_CURVE('',#1291,#1291,#801,.T.);
#1596=EDGE_CURVE('',#1292,#1292,#802,.T.);
#1597=EDGE_CURVE('',#1293,#1294,#935,.T.);
#1598=EDGE_CURVE('',#1294,#1295,#936,.T.);
#1599=EDGE_CURVE('',#1295,#1296,#937,.T.);
#1600=EDGE_CURVE('',#1296,#1297,#938,.T.);
#1601=EDGE_CURVE('',#1297,#1298,#939,.T.);
#1602=EDGE_CURVE('',#1298,#1293,#940,.T.);
#1603=EDGE_CURVE('',#1299,#1282,#941,.T.);
#1604=EDGE_CURVE('',#1282,#1300,#942,.T.);
#1605=EDGE_CURVE('',#1300,#1295,#943,.T.);
#1606=EDGE_CURVE('',#1299,#1294,#944,.T.);
#1607=EDGE_CURVE('',#1300,#1281,#945,.T.);
#1608=EDGE_CURVE('',#1281,#1301,#946,.T.);
#1609=EDGE_CURVE('',#1301,#1296,#947,.T.);
#1610=EDGE_CURVE('',#1301,#1280,#948,.T.);
#1611=EDGE_CURVE('',#1280,#1302,#949,.T.);
#1612=EDGE_CURVE('',#1302,#1297,#950,.T.);
#1613=EDGE_CURVE('',#1302,#1285,#951,.T.);
#1614=EDGE_CURVE('',#1285,#1303,#952,.T.);
#1615=EDGE_CURVE('',#1303,#1298,#953,.T.);
#1616=EDGE_CURVE('',#1303,#1284,#954,.T.);
#1617=EDGE_CURVE('',#1284,#1304,#955,.T.);
#1618=EDGE_CURVE('',#1304,#1293,#956,.T.);
#1619=EDGE_CURVE('',#1304,#1283,#957,.T.);
#1620=EDGE_CURVE('',#1283,#1299,#958,.T.);
#2169=ORIENTED_EDGE('',*,*,#1579,.T.);
#2170=ORIENTED_EDGE('',*,*,#1580,.T.);
#2171=ORIENTED_EDGE('',*,*,#1581,.T.);
#2172=ORIENTED_EDGE('',*,*,#1582,.T.);
#2173=ORIENTED_EDGE('',*,*,#1583,.T.);
#2174=ORIENTED_EDGE('',*,*,#1584,.T.);
#2175=ORIENTED_EDGE('',*,*,#1585,.T.);
#2176=ORIENTED_EDGE('',*,*,#1579,.F.);
#2177=ORIENTED_EDGE('',*,*,#1586,.F.);
#2178=ORIENTED_EDGE('',*,*,#1587,.T.);
#2179=ORIENTED_EDGE('',*,*,#1588,.F.);
#2180=ORIENTED_EDGE('',*,*,#1587,.F.);
#2181=ORIENTED_EDGE('',*,*,#1589,.F.);
#2182=ORIENTED_EDGE('',*,*,#1590,.T.);
#2183=ORIENTED_EDGE('',*,*,#1591,.T.);
#2184=ORIENTED_EDGE('',*,*,#1590,.F.);
#2185=ORIENTED_EDGE('',*,*,#1588,.T.);
#2186=ORIENTED_EDGE('',*,*,#1592,.T.);
#2187=ORIENTED_EDGE('',*,*,#1589,.T.);
#2188=ORIENTED_EDGE('',*,*,#1592,.F.);
#2189=ORIENTED_EDGE('',*,*,#1593,.F.);
#2190=ORIENTED_EDGE('',*,*,#1594,.T.);
#2191=ORIENTED_EDGE('',*,*,#1595,.T.);
#2192=ORIENTED_EDGE('',*,*,#1594,.F.);
#2193=ORIENTED_EDGE('',*,*,#1593,.T.);
#2194=ORIENTED_EDGE('',*,*,#1596,.F.);
#2195=ORIENTED_EDGE('',*,*,#1596,.T.);
#2196=ORIENTED_EDGE('',*,*,#1597,.T.);
#2197=ORIENTED_EDGE('',*,*,#1598,.T.);
#2198=ORIENTED_EDGE('',*,*,#1599,.T.);
#2199=ORIENTED_EDGE('',*,*,#1600,.T.);
#2200=ORIENTED_EDGE('',*,*,#1601,.T.);
#2201=ORIENTED_EDGE('',*,*,#1602,.T.);
#2202=ORIENTED_EDGE('',*,*,#1595,.F.);
#2203=ORIENTED_EDGE('',*,*,#1586,.T.);
#2204=ORIENTED_EDGE('',*,*,#1591,.F.);
#2205=ORIENTED_EDGE('',*,*,#1603,.T.);
#2206=ORIENTED_EDGE('',*,*,#1604,.T.);
#2207=ORIENTED_EDGE('',*,*,#1605,.T.);
#2208=ORIENTED_EDGE('',*,*,#1598,.F.);
#2209=ORIENTED_EDGE('',*,*,#1606,.F.);
#2210=ORIENTED_EDGE('',*,*,#1607,.T.);
#2211=ORIENTED_EDGE('',*,*,#1608,.T.);
#2212=ORIENTED_EDGE('',*,*,#1609,.T.);
#2213=ORIENTED_EDGE('',*,*,#1599,.F.);
#2214=ORIENTED_EDGE('',*,*,#1605,.F.);
#2215=ORIENTED_EDGE('',*,*,#1610,.T.);
#2216=ORIENTED_EDGE('',*,*,#1611,.T.);
#2217=ORIENTED_EDGE('',*,*,#1612,.T.);
#2218=ORIENTED_EDGE('',*,*,#1600,.F.);
#2219=ORIENTED_EDGE('',*,*,#1609,.F.);
#2220=ORIENTED_EDGE('',*,*,#1613,.T.);
#2221=ORIENTED_EDGE('',*,*,#1614,.T.);
#2222=ORIENTED_EDGE('',*,*,#1615,.T.);
#2223=ORIENTED_EDGE('',*,*,#1601,.F.);
#2224=ORIENTED_EDGE('',*,*,#1612,.F.);
#2225=ORIENTED_EDGE('',*,*,#1616,.T.);
#2226=ORIENTED_EDGE('',*,*,#1617,.T.);
#2227=ORIENTED_EDGE('',*,*,#1618,.T.);
#2228=ORIENTED_EDGE('',*,*,#1602,.F.);
#2229=ORIENTED_EDGE('',*,*,#1615,.F.);
#2230=ORIENTED_EDGE('',*,*,#1619,.T.);
#2231=ORIENTED_EDGE('',*,*,#1620,.T.);
#2232=ORIENTED_EDGE('',*,*,#1606,.T.);
#2233=ORIENTED_EDGE('',*,*,#1597,.F.);
#2234=ORIENTED_EDGE('',*,*,#1618,.F.);
#2235=ORIENTED_EDGE('',*,*,#1585,.F.);
#2236=ORIENTED_EDGE('',*,*,#1613,.F.);
#2237=ORIENTED_EDGE('',*,*,#1611,.F.);
#2238=ORIENTED_EDGE('',*,*,#1584,.F.);
#2239=ORIENTED_EDGE('',*,*,#1616,.F.);
#2240=ORIENTED_EDGE('',*,*,#1614,.F.);
#2241=ORIENTED_EDGE('',*,*,#1583,.F.);
#2242=ORIENTED_EDGE('',*,*,#1619,.F.);
#2243=ORIENTED_EDGE('',*,*,#1617,.F.);
#2244=ORIENTED_EDGE('',*,*,#1582,.F.);
#2245=ORIENTED_EDGE('',*,*,#1603,.F.);
#2246=ORIENTED_EDGE('',*,*,#1620,.F.);
#2247=ORIENTED_EDGE('',*,*,#1581,.F.);
#2248=ORIENTED_EDGE('',*,*,#1607,.F.);
#2249=ORIENTED_EDGE('',*,*,#1604,.F.);
#2250=ORIENTED_EDGE('',*,*,#1580,.F.);
#2251=ORIENTED_EDGE('',*,*,#1610,.F.);
#2252=ORIENTED_EDGE('',*,*,#1608,.F.);
#2257=CONICAL_SURFACE('',#2817,1732.05080756886,1.04719755119659);
#2258=CONICAL_SURFACE('',#2828,1.61,0.785398163397447);
#2392=ADVANCED_FACE('',(#441),#2257,.F.);
#2393=ADVANCED_FACE('',(#442),#90,.F.);
#2394=ADVANCED_FACE('',(#443),#2258,.T.);
#2395=ADVANCED_FACE('',(#444),#306,.T.);
#2396=ADVANCED_FACE('',(#445),#307,.T.);
#2397=ADVANCED_FACE('',(#446,#188),#59,.T.);
#2398=ADVANCED_FACE('',(#447,#189),#237,.T.);
#2399=ADVANCED_FACE('',(#448,#190),#238,.F.);
#2400=ADVANCED_FACE('',(#449),#239,.F.);
#2401=ADVANCED_FACE('',(#450),#240,.T.);
#2402=ADVANCED_FACE('',(#451),#241,.T.);
#2403=ADVANCED_FACE('',(#452),#242,.T.);
#2404=ADVANCED_FACE('',(#453),#243,.T.);
#2405=ADVANCED_FACE('',(#454),#244,.T.);
#2406=ADVANCED_FACE('',(#455),#245,.T.);
#2407=ADVANCED_FACE('',(#456),#246,.F.);
#2408=ADVANCED_FACE('',(#457),#247,.F.);
#2409=ADVANCED_FACE('',(#458),#248,.F.);
#2410=ADVANCED_FACE('',(#459),#249,.F.);
#2411=ADVANCED_FACE('',(#460),#250,.F.);
#2412=ADVANCED_FACE('',(#461),#251,.F.);
#2433=CLOSED_SHELL('',(#2392,#2393,#2394,#2395,#2396,#2397,#2398,#2399,
#2400,#2401,#2402,#2403,#2404,#2405,#2406,#2407,#2408,#2409,#2410,#2411,
#2412));
#2816=AXIS2_PLACEMENT_3D('',#7504,#3556,#3557);
#2817=AXIS2_PLACEMENT_3D('',#7505,#3558,#3559);
#2818=AXIS2_PLACEMENT_3D('',#7510,#3561,#3562);
#2819=AXIS2_PLACEMENT_3D('',#7512,#3563,#3564);
#2820=AXIS2_PLACEMENT_3D('',#7514,#3565,#3566);
#2821=AXIS2_PLACEMENT_3D('',#7516,#3567,#3568);
#2822=AXIS2_PLACEMENT_3D('',#7518,#3569,#3570);
#2823=AXIS2_PLACEMENT_3D('',#7519,#3571,#3572);
#2824=AXIS2_PLACEMENT_3D('',#7520,#3573,#3574);
#2825=AXIS2_PLACEMENT_3D('',#7522,#3575,#3576);
#2826=AXIS2_PLACEMENT_3D('',#7524,#3577,#3578);
#2827=AXIS2_PLACEMENT_3D('',#7525,#3579,#3580);
#2828=AXIS2_PLACEMENT_3D('',#7526,#3581,#3582);
#2829=AXIS2_PLACEMENT_3D('',#7528,#3583,#3584);
#2830=AXIS2_PLACEMENT_3D('',#7531,#3586,#3587);
#2831=AXIS2_PLACEMENT_3D('',#7532,#3588,#3589);
#2832=AXIS2_PLACEMENT_3D('',#7534,#3591,#3592);
#2833=AXIS2_PLACEMENT_3D('',#7536,#3593,#3594);
#2834=AXIS2_PLACEMENT_3D('',#7539,#3596,#3597);
#2835=AXIS2_PLACEMENT_3D('',#7540,#3598,#3599);
#2836=AXIS2_PLACEMENT_3D('',#7542,#3600,#3601);
#2837=AXIS2_PLACEMENT_3D('',#7543,#3602,#3603);
#2838=AXIS2_PLACEMENT_3D('',#7556,#3610,#3611);
#2839=AXIS2_PLACEMENT_3D('',#7557,#3612,#3613);
#2840=AXIS2_PLACEMENT_3D('',#7558,#3614,#3615);
#2841=AXIS2_PLACEMENT_3D('',#7565,#3620,#3621);
#2842=AXIS2_PLACEMENT_3D('',#7570,#3625,#3626);
#2843=AXIS2_PLACEMENT_3D('',#7575,#3630,#3631);
#2844=AXIS2_PLACEMENT_3D('',#7580,#3635,#3636);
#2845=AXIS2_PLACEMENT_3D('',#7585,#3640,#3641);
#2846=AXIS2_PLACEMENT_3D('',#7588,#3644,#3645);
#2847=AXIS2_PLACEMENT_3D('',#7589,#3646,#3647);
#2848=AXIS2_PLACEMENT_3D('',#7590,#3648,#3649);
#2849=AXIS2_PLACEMENT_3D('',#7591,#3650,#3651);
#2850=AXIS2_PLACEMENT_3D('',#7592,#3652,#3653);
#2851=AXIS2_PLACEMENT_3D('',#7593,#3654,#3655);
#3556=DIRECTION('axis',(0.,0.,1.));
#3557=DIRECTION('refdir',(1.,0.,0.));
#3558=DIRECTION('center_axis',(-1.,0.,0.));
#3559=DIRECTION('ref_axis',(0.,0.,1.));
#3560=DIRECTION('',(-0.500000000000004,-1.0605752387249E-16,-0.866025403784436));
#3561=DIRECTION('center_axis',(-1.,0.,0.));
#3562=DIRECTION('ref_axis',(0.,0.,1.));
#3563=DIRECTION('center_axis',(-1.,0.,0.));
#3564=DIRECTION('ref_axis',(0.,0.,1.));
#3565=DIRECTION('center_axis',(-1.,0.,0.));
#3566=DIRECTION('ref_axis',(0.,0.,1.));
#3567=DIRECTION('center_axis',(-1.,0.,0.));
#3568=DIRECTION('ref_axis',(0.,0.,1.));
#3569=DIRECTION('center_axis',(-1.,0.,0.));
#3570=DIRECTION('ref_axis',(0.,0.,1.));
#3571=DIRECTION('center_axis',(-1.,0.,0.));
#3572=DIRECTION('ref_axis',(0.,0.,1.));
#3573=DIRECTION('center_axis',(-1.,0.,0.));
#3574=DIRECTION('ref_axis',(0.,0.,1.));
#3575=DIRECTION('center_axis',(-1.,0.,0.));
#3576=DIRECTION('ref_axis',(0.,0.,1.));
#3577=DIRECTION('center_axis',(0.,1.,-1.22464679914735E-16));
#3578=DIRECTION('ref_axis',(0.,-1.22464679914735E-16,-1.));
#3579=DIRECTION('center_axis',(1.,0.,0.));
#3580=DIRECTION('ref_axis',(0.,0.,1.));
#3581=DIRECTION('center_axis',(-1.,0.,0.));
#3582=DIRECTION('ref_axis',(0.,0.,1.));
#3583=DIRECTION('center_axis',(-1.,0.,0.));
#3584=DIRECTION('ref_axis',(0.,0.,1.));
#3585=DIRECTION('',(0.707106781186549,8.65956056235492E-17,0.707106781186547));
#3586=DIRECTION('center_axis',(-1.,0.,0.));
#3587=DIRECTION('ref_axis',(0.,0.,1.));
#3588=DIRECTION('center_axis',(-1.,0.,0.));
#3589=DIRECTION('ref_axis',(0.,0.,1.));
#3590=DIRECTION('',(1.,0.,0.));
#3591=DIRECTION('center_axis',(-1.,0.,0.));
#3592=DIRECTION('ref_axis',(0.,0.,1.));
#3593=DIRECTION('center_axis',(-1.,0.,0.));
#3594=DIRECTION('ref_axis',(0.,0.,1.));
#3595=DIRECTION('',(1.,0.,0.));
#3596=DIRECTION('center_axis',(-1.,0.,0.));
#3597=DIRECTION('ref_axis',(0.,0.,1.));
#3598=DIRECTION('center_axis',(0.,6.12323399573677E-17,-1.));
#3599=DIRECTION('ref_axis',(0.,1.,0.));
#3600=DIRECTION('center_axis',(-1.,0.,0.));
#3601=DIRECTION('ref_axis',(0.,0.,1.));
#3602=DIRECTION('center_axis',(-1.,0.,0.));
#3603=DIRECTION('ref_axis',(0.,0.,1.));
#3604=DIRECTION('',(0.,-1.,1.50231459873716E-16));
#3605=DIRECTION('',(0.,-0.5,-0.866025403784438));
#3606=DIRECTION('',(0.,0.5,-0.866025403784438));
#3607=DIRECTION('',(0.,1.,0.));
#3608=DIRECTION('',(0.,0.5,0.866025403784439));
#3609=DIRECTION('',(0.,-0.5,0.866025403784438));
#3610=DIRECTION('center_axis',(-1.,0.,0.));
#3611=DIRECTION('ref_axis',(0.,0.,1.));
#3612=DIRECTION('center_axis',(-1.,0.,0.));
#3613=DIRECTION('ref_axis',(0.,0.,1.));
#3614=DIRECTION('center_axis',(0.,0.866025403784439,-0.5));
#3615=DIRECTION('ref_axis',(0.,0.5,0.866025403784439));
#3616=DIRECTION('',(0.,-0.5,-0.866025403784438));
#3617=DIRECTION('',(0.,-0.5,-0.866025403784438));
#3618=DIRECTION('',(-1.,0.,0.));
#3619=DIRECTION('',(-1.,0.,0.));
#3620=DIRECTION('center_axis',(0.,0.866025403784439,0.5));
#3621=DIRECTION('ref_axis',(0.,-0.5,0.866025403784439));
#3622=DIRECTION('',(0.,0.5,-0.866025403784438));
#3623=DIRECTION('',(0.,0.5,-0.866025403784438));
#3624=DIRECTION('',(-1.,0.,0.));
#3625=DIRECTION('center_axis',(0.,0.,1.));
#3626=DIRECTION('ref_axis',(1.,0.,0.));
#3627=DIRECTION('',(0.,1.,0.));
#3628=DIRECTION('',(0.,1.,0.));
#3629=DIRECTION('',(-1.,0.,0.));
#3630=DIRECTION('center_axis',(0.,-0.866025403784439,0.5));
#3631=DIRECTION('ref_axis',(0.,-0.5,-0.866025403784439));
#3632=DIRECTION('',(0.,0.5,0.866025403784439));
#3633=DIRECTION('',(0.,0.5,0.866025403784439));
#3634=DIRECTION('',(-1.,0.,0.));
#3635=DIRECTION('center_axis',(0.,-0.866025403784439,-0.5));
#3636=DIRECTION('ref_axis',(0.,0.5,-0.866025403784439));
#3637=DIRECTION('',(0.,-0.5,0.866025403784438));
#3638=DIRECTION('',(0.,-0.5,0.866025403784438));
#3639=DIRECTION('',(-1.,0.,0.));
#3640=DIRECTION('center_axis',(0.,-1.50231459873716E-16,-1.));
#3641=DIRECTION('ref_axis',(0.,1.,-1.50231459873716E-16));
#3642=DIRECTION('',(0.,-1.,1.50231459873716E-16));
#3643=DIRECTION('',(0.,-1.,1.50231459873716E-16));
#3644=DIRECTION('center_axis',(1.,0.,0.));
#3645=DIRECTION('ref_axis',(0.,0.,-1.));
#3646=DIRECTION('center_axis',(1.,0.,0.));
#3647=DIRECTION('ref_axis',(0.,0.,-1.));
#3648=DIRECTION('center_axis',(1.,0.,0.));
#3649=DIRECTION('ref_axis',(0.,0.,-1.));
#3650=DIRECTION('center_axis',(1.,0.,0.));
#3651=DIRECTION('ref_axis',(0.,0.,-1.));
#3652=DIRECTION('center_axis',(1.,0.,0.));
#3653=DIRECTION('ref_axis',(0.,0.,-1.));
#3654=DIRECTION('center_axis',(1.,0.,0.));
#3655=DIRECTION('ref_axis',(0.,0.,-1.));
#7504=CARTESIAN_POINT('',(0.,0.,0.));
#7505=CARTESIAN_POINT('Origin',(-997.978312163513,0.,0.));
#7506=CARTESIAN_POINT('',(2.02168783648704,2.16840434497101E-16,0.));
#7507=CARTESIAN_POINT('',(1.3,0.,-1.25));
#7508=CARTESIAN_POINT('',(-997.978312163513,-2.12115047744979E-13,-1732.05080756886));
#7509=CARTESIAN_POINT('',(1.3,-1.08253175473055,-0.625));
#7510=CARTESIAN_POINT('Origin',(1.3,0.,0.));
#7511=CARTESIAN_POINT('',(1.3,-1.08253175473055,0.625));
#7512=CARTESIAN_POINT('Origin',(1.3,0.,0.));
#7513=CARTESIAN_POINT('',(1.3,1.87789324842145E-16,1.25));
#7514=CARTESIAN_POINT('Origin',(1.3,0.,0.));
#7515=CARTESIAN_POINT('',(1.3,1.08253175473055,0.625000000000001));
#7516=CARTESIAN_POINT('Origin',(1.3,0.,0.));
#7517=CARTESIAN_POINT('',(1.3,1.08253175473055,-0.625));
#7518=CARTESIAN_POINT('Origin',(1.3,0.,0.));
#7519=CARTESIAN_POINT('Origin',(1.3,0.,0.));
#7520=CARTESIAN_POINT('Origin',(2.4,0.,0.));
#7521=CARTESIAN_POINT('',(2.2,-2.69422295812418E-16,-2.2));
#7522=CARTESIAN_POINT('Origin',(2.2,0.,0.));
#7523=CARTESIAN_POINT('',(2.4,-2.44929359829471E-16,-2.));
#7524=CARTESIAN_POINT('Origin',(2.4,-2.69422295812418E-16,-2.2));
#7525=CARTESIAN_POINT('Origin',(2.4,0.,0.));
#7526=CARTESIAN_POINT('Origin',(14.2,0.,0.));
#7527=CARTESIAN_POINT('',(13.81,-2.44929359829471E-16,-2.));
#7528=CARTESIAN_POINT('Origin',(13.81,0.,0.));
#7529=CARTESIAN_POINT('',(14.2,-1.97168134662724E-16,-1.61));
#7530=CARTESIAN_POINT('',(14.2,-1.97168134662724E-16,-1.61));
#7531=CARTESIAN_POINT('Origin',(14.2,0.,0.));
#7532=CARTESIAN_POINT('Origin',(0.,0.,0.));
#7533=CARTESIAN_POINT('',(0.,-2.44929359829471E-16,-2.));
#7534=CARTESIAN_POINT('Origin',(0.,0.,0.));
#7535=CARTESIAN_POINT('',(1.82,-4.65365783675994E-16,-3.8));
#7536=CARTESIAN_POINT('Origin',(1.82,0.,0.));
#7537=CARTESIAN_POINT('',(2.2,-4.65365783675994E-16,-3.8));
#7538=CARTESIAN_POINT('',(0.,-4.65365783675994E-16,-3.8));
#7539=CARTESIAN_POINT('Origin',(2.2,0.,0.));
#7540=CARTESIAN_POINT('Origin',(3.88527472527473,-4.33680868994202E-16,
0.));
#7541=CARTESIAN_POINT('',(8.67361737988404E-16,1.9,0.));
#7542=CARTESIAN_POINT('Origin',(8.67361737988404E-16,0.,0.));
#7543=CARTESIAN_POINT('Origin',(4.33680868994202E-16,0.,0.));
#7544=CARTESIAN_POINT('',(0.,0.721687836487033,1.25));
#7545=CARTESIAN_POINT('',(4.33680868994202E-16,-0.721687836487032,1.25));
#7546=CARTESIAN_POINT('',(0.,-0.721687836487032,1.25));
#7547=CARTESIAN_POINT('',(0.,-1.44337567297406,1.27850268845987E-18));
#7548=CARTESIAN_POINT('',(0.,-1.44337567297406,1.27850268845987E-18));
#7549=CARTESIAN_POINT('',(0.,-0.721687836487032,-1.25));
#7550=CARTESIAN_POINT('',(0.,-0.721687836487032,-1.25));
#7551=CARTESIAN_POINT('',(0.,0.721687836487033,-1.25));
#7552=CARTESIAN_POINT('',(0.,0.721687836487033,-1.25));
#7553=CARTESIAN_POINT('',(0.,1.44337567297407,7.22223729145213E-31));
#7554=CARTESIAN_POINT('',(0.,1.44337567297407,7.22223729145213E-31));
#7555=CARTESIAN_POINT('',(0.,0.721687836487033,1.25));
#7556=CARTESIAN_POINT('Origin',(2.2,2.,0.));
#7557=CARTESIAN_POINT('Origin',(14.2,0.,0.));
#7558=CARTESIAN_POINT('Origin',(1.3,-1.44337567297406,1.27850268845987E-18));
#7559=CARTESIAN_POINT('',(1.3,-0.721687836487032,1.25));
#7560=CARTESIAN_POINT('',(1.3,-1.44337567297406,1.27850268845987E-18));
#7561=CARTESIAN_POINT('',(1.3,-1.44337567297406,1.27850268845987E-18));
#7562=CARTESIAN_POINT('',(1.3,-1.44337567297406,1.27850268845987E-18));
#7563=CARTESIAN_POINT('',(1.3,-1.44337567297406,1.27850268845987E-18));
#7564=CARTESIAN_POINT('',(1.3,-0.721687836487032,1.25));
#7565=CARTESIAN_POINT('Origin',(1.3,-0.721687836487032,-1.25));
#7566=CARTESIAN_POINT('',(1.3,-0.721687836487032,-1.25));
#7567=CARTESIAN_POINT('',(1.3,-0.721687836487032,-1.25));
#7568=CARTESIAN_POINT('',(1.3,-0.721687836487032,-1.25));
#7569=CARTESIAN_POINT('',(1.3,-0.721687836487032,-1.25));
#7570=CARTESIAN_POINT('Origin',(1.3,0.721687836487033,-1.25));
#7571=CARTESIAN_POINT('',(1.3,0.721687836487033,-1.25));
#7572=CARTESIAN_POINT('',(1.3,0.721687836487033,-1.25));
#7573=CARTESIAN_POINT('',(1.3,0.721687836487033,-1.25));
#7574=CARTESIAN_POINT('',(1.3,0.721687836487033,-1.25));
#7575=CARTESIAN_POINT('Origin',(1.3,1.44337567297407,7.22223729145213E-31));
#7576=CARTESIAN_POINT('',(1.3,1.44337567297407,7.22223729145213E-31));
#7577=CARTESIAN_POINT('',(1.3,1.44337567297407,7.22223729145213E-31));
#7578=CARTESIAN_POINT('',(1.3,1.44337567297407,7.22223729145213E-31));
#7579=CARTESIAN_POINT('',(1.3,1.44337567297407,7.22223729145213E-31));
#7580=CARTESIAN_POINT('Origin',(1.3,0.721687836487033,1.25));
#7581=CARTESIAN_POINT('',(1.3,0.721687836487033,1.25));
#7582=CARTESIAN_POINT('',(1.3,0.721687836487033,1.25));
#7583=CARTESIAN_POINT('',(1.3,0.721687836487033,1.25));
#7584=CARTESIAN_POINT('',(1.3,0.721687836487033,1.25));
#7585=CARTESIAN_POINT('Origin',(1.3,-0.721687836487032,1.25));
#7586=CARTESIAN_POINT('',(1.3,-0.721687836487032,1.25));
#7587=CARTESIAN_POINT('',(1.3,-0.721687836487032,1.25));
#7588=CARTESIAN_POINT('Origin',(1.3,-1.44337567297406,2.16840434497101E-16));
#7589=CARTESIAN_POINT('Origin',(1.3,-1.44337567297406,2.16840434497101E-16));
#7590=CARTESIAN_POINT('Origin',(1.3,-1.44337567297406,2.16840434497101E-16));
#7591=CARTESIAN_POINT('Origin',(1.3,-1.44337567297406,2.16840434497101E-16));
#7592=CARTESIAN_POINT('Origin',(1.3,-1.44337567297406,2.16840434497101E-16));
#7593=CARTESIAN_POINT('Origin',(1.3,-1.44337567297406,2.16840434497101E-16));
#7615=UNCERTAINTY_MEASURE_WITH_UNIT(LENGTH_MEASURE(0.01),#7628,
'DISTANCE_ACCURACY_VALUE',
'Maximum model space distance between geometric entities at asserted c
onnectivities');
#7616=UNCERTAINTY_MEASURE_WITH_UNIT(LENGTH_MEASURE(0.01),#7628,
'DISTANCE_ACCURACY_VALUE',
'Maximum model space distance between geometric entities at asserted c
onnectivities');
#7626=(
GEOMETRIC_REPRESENTATION_CONTEXT(3)
GLOBAL_UNCERTAINTY_ASSIGNED_CONTEXT((#7615))
GLOBAL_UNIT_ASSIGNED_CONTEXT((#7628,#7630,#7631))
REPRESENTATION_CONTEXT('','3D')
);
#7627=(
GEOMETRIC_REPRESENTATION_CONTEXT(3)
GLOBAL_UNCERTAINTY_ASSIGNED_CONTEXT((#7616))
GLOBAL_UNIT_ASSIGNED_CONTEXT((#7628,#7630,#7631))
REPRESENTATION_CONTEXT('','3D')
);
#7628=(
LENGTH_UNIT()
NAMED_UNIT(*)
SI_UNIT(.MILLI.,.METRE.)
);
#7630=(
NAMED_UNIT(*)
PLANE_ANGLE_UNIT()
SI_UNIT($,.RADIAN.)
);
#7631=(
NAMED_UNIT(*)
SI_UNIT($,.STERADIAN.)
SOLID_ANGLE_UNIT()
);
#7641=SHAPE_DEFINITION_REPRESENTATION(#7651,#7673);
#7651=PRODUCT_DEFINITION_SHAPE('',$,#7684);
#7673=SHAPE_REPRESENTATION('',(#2816),#7626);
#7674=PRODUCT_DEFINITION_CONTEXT('part definition',#7706,'design');
#7684=PRODUCT_DEFINITION(
'socket button head screw_iso_ISO 7380 - M4 x 12 - 12N',
'socket button head screw_iso_ISO 7380 - M4 x 12 - 12N',#7694,#7674);
#7694=PRODUCT_DEFINITION_FORMATION('',$,#7717);
#7706=APPLICATION_CONTEXT(
'Core Data for Automotive Mechanical Design Process');
#7707=PRODUCT_CONTEXT('part definition',#7706,'mechanical');
#7717=PRODUCT('socket button head screw_iso_ISO 7380 - M4 x 12 - 12N',
'socket button head screw_iso_ISO 7380 - M4 x 12 - 12N',$,(#7707));
#7721=PRESENTATION_STYLE_ASSIGNMENT((#7727));
#7727=SURFACE_STYLE_USAGE(.BOTH.,#7733);
#7733=SURFACE_SIDE_STYLE('',(#7739));
#7739=SURFACE_STYLE_FILL_AREA(#7745);
#7745=FILL_AREA_STYLE('Opaque(31,36,43)',(#7751));
#7751=FILL_AREA_STYLE_COLOUR('Opaque(31,36,43)',#7757);
#7757=COLOUR_RGB('Opaque(31,36,43)',0.12156862745098,0.141176470588235,
0.168627450980392);
ENDSEC;
END-ISO-10303-21;
